ISO-10303-21;
HEADER;
/* Generated by software containing ST-Developer
 * from STEP Tools, Inc. (www.steptools.com) 
 */

FILE_DESCRIPTION(
/* description */ ('PAT-015'),
/* implementation_level */ '2;1');

FILE_NAME(
/* name */ 'Gauge dummy.step',
/* time_stamp */ '2026-10-29T16:03:43-07:00',
/* author */ (''),
/* organization */ (''),
/* preprocessor_version */ 'ST-DEVELOPER v20.2',
/* originating_system */ 'Autodesk Translation Framework v15.17.0.0',
/* authorisation */ '');

FILE_SCHEMA (('AUTOMOTIVE_DESIGN { 1 0 10303 214 3 1 1 }'));
ENDSEC;

DATA;
#10=MECHANICAL_DESIGN_GEOMETRIC_PRESENTATION_REPRESENTATION('',(#233,#234,#235),#10266);
#187=SHAPE_REPRESENTATION_RELATIONSHIP('SRR','None',#10358,#210);
#210=ADVANCED_BREP_SHAPE_REPRESENTATION('',(#258,#259,#260),#10246);
#233=STYLED_ITEM('',(#10561),#258);
#234=STYLED_ITEM('',(#10561),#259);
#235=STYLED_ITEM('',(#10561),#260);
#258=MANIFOLD_SOLID_BREP('Body1',#4692);
#259=MANIFOLD_SOLID_BREP('Off white dial',#4693);
#260=MANIFOLD_SOLID_BREP('Black pointer',#4694);
#345=FACE_BOUND('',#994,.T.);
#455=PLANE('',#5145);
#456=PLANE('',#5150);
#457=PLANE('',#5153);
#458=PLANE('',#5157);
#459=PLANE('',#5158);
#460=PLANE('',#5159);
#461=PLANE('',#5160);
#462=PLANE('',#5161);
#463=PLANE('',#5162);
#464=PLANE('',#5163);
#465=PLANE('',#5164);
#466=PLANE('',#5165);
#657=FACE_OUTER_BOUND('',#993,.T.);
#658=FACE_OUTER_BOUND('',#995,.T.);
#659=FACE_OUTER_BOUND('',#996,.T.);
#660=FACE_OUTER_BOUND('',#997,.T.);
#661=FACE_OUTER_BOUND('',#998,.T.);
#662=FACE_OUTER_BOUND('',#999,.T.);
#663=FACE_OUTER_BOUND('',#1000,.T.);
#664=FACE_OUTER_BOUND('',#1001,.T.);
#665=FACE_OUTER_BOUND('',#1002,.T.);
#666=FACE_OUTER_BOUND('',#1003,.T.);
#667=FACE_OUTER_BOUND('',#1004,.T.);
#668=FACE_OUTER_BOUND('',#1005,.T.);
#669=FACE_OUTER_BOUND('',#1006,.T.);
#670=FACE_OUTER_BOUND('',#1007,.T.);
#671=FACE_OUTER_BOUND('',#1008,.T.);
#993=EDGE_LOOP('',(#3505));
#994=EDGE_LOOP('',(#3506));
#995=EDGE_LOOP('',(#3507,#3508,#3509,#3510));
#996=EDGE_LOOP('',(#3511));
#997=EDGE_LOOP('',(#3512,#3513,#3514,#3515));
#998=EDGE_LOOP('',(#3516));
#999=EDGE_LOOP('',(#3517,#3518,#3519,#3520));
#1000=EDGE_LOOP('',(#3521));
#1001=EDGE_LOOP('',(#3522));
#1002=EDGE_LOOP('',(#3523,#3524,#3525,#3526));
#1003=EDGE_LOOP('',(#3527,#3528,#3529,#3530));
#1004=EDGE_LOOP('',(#3531,#3532,#3533,#3534));
#1005=EDGE_LOOP('',(#3535,#3536,#3537,#3538));
#1006=EDGE_LOOP('',(#3539,#3540,#3541,#3542));
#1007=EDGE_LOOP('',(#3543,#3544,#3545,#3546,#3547));
#1008=EDGE_LOOP('',(#3548,#3549,#3550,#3551,#3552));
#1387=LINE('',#8469,#1667);
#1388=LINE('',#8475,#1668);
#1389=LINE('',#8481,#1669);
#1390=LINE('',#8488,#1670);
#1391=LINE('',#8490,#1671);
#1392=LINE('',#8492,#1672);
#1393=LINE('',#8493,#1673);
#1394=LINE('',#8496,#1674);
#1395=LINE('',#8498,#1675);
#1396=LINE('',#8499,#1676);
#1397=LINE('',#8502,#1677);
#1398=LINE('',#8504,#1678);
#1399=LINE('',#8505,#1679);
#1400=LINE('',#8508,#1680);
#1401=LINE('',#8510,#1681);
#1402=LINE('',#8511,#1682);
#1403=LINE('',#8513,#1683);
#1404=LINE('',#8514,#1684);
#1667=VECTOR('',#5978,2.);
#1668=VECTOR('',#5987,0.685);
#1669=VECTOR('',#5994,1.9);
#1670=VECTOR('',#6003,1.);
#1671=VECTOR('',#6004,1.);
#1672=VECTOR('',#6005,1.);
#1673=VECTOR('',#6006,1.);
#1674=VECTOR('',#6009,1.);
#1675=VECTOR('',#6010,1.);
#1676=VECTOR('',#6011,1.);
#1677=VECTOR('',#6014,1.);
#1678=VECTOR('',#6015,1.);
#1679=VECTOR('',#6016,1.);
#1680=VECTOR('',#6019,1.);
#1681=VECTOR('',#6020,1.);
#1682=VECTOR('',#6021,1.);
#1683=VECTOR('',#6024,1.);
#1684=VECTOR('',#6025,1.);
#1953=CIRCLE('',#5146,2.);
#1954=CIRCLE('',#5147,0.685);
#1955=CIRCLE('',#5149,2.);
#1956=CIRCLE('',#5152,0.685);
#1957=CIRCLE('',#5155,1.9);
#1958=CIRCLE('',#5156,1.9);
#2249=VERTEX_POINT('',#8463);
#2250=VERTEX_POINT('',#8465);
#2251=VERTEX_POINT('',#8468);
#2252=VERTEX_POINT('',#8473);
#2253=VERTEX_POINT('',#8478);
#2254=VERTEX_POINT('',#8480);
#2255=VERTEX_POINT('',#8486);
#2256=VERTEX_POINT('',#8487);
#2257=VERTEX_POINT('',#8489);
#2258=VERTEX_POINT('',#8491);
#2259=VERTEX_POINT('',#8495);
#2260=VERTEX_POINT('',#8497);
#2261=VERTEX_POINT('',#8501);
#2262=VERTEX_POINT('',#8503);
#2263=VERTEX_POINT('',#8507);
#2264=VERTEX_POINT('',#8509);
#2708=EDGE_CURVE('',#2249,#2249,#1953,.T.);
#2709=EDGE_CURVE('',#2250,#2250,#1954,.T.);
#2710=EDGE_CURVE('',#2249,#2251,#1387,.T.);
#2711=EDGE_CURVE('',#2251,#2251,#1955,.T.);
#2712=EDGE_CURVE('',#2252,#2252,#1956,.T.);
#2713=EDGE_CURVE('',#2252,#2250,#1388,.T.);
#2714=EDGE_CURVE('',#2253,#2253,#1957,.T.);
#2715=EDGE_CURVE('',#2253,#2254,#1389,.T.);
#2716=EDGE_CURVE('',#2254,#2254,#1958,.T.);
#2717=EDGE_CURVE('',#2255,#2256,#1390,.T.);
#2718=EDGE_CURVE('',#2255,#2257,#1391,.T.);
#2719=EDGE_CURVE('',#2258,#2257,#1392,.T.);
#2720=EDGE_CURVE('',#2256,#2258,#1393,.T.);
#2721=EDGE_CURVE('',#2256,#2259,#1394,.T.);
#2722=EDGE_CURVE('',#2260,#2258,#1395,.T.);
#2723=EDGE_CURVE('',#2259,#2260,#1396,.T.);
#2724=EDGE_CURVE('',#2259,#2261,#1397,.T.);
#2725=EDGE_CURVE('',#2262,#2260,#1398,.T.);
#2726=EDGE_CURVE('',#2261,#2262,#1399,.T.);
#2727=EDGE_CURVE('',#2261,#2263,#1400,.T.);
#2728=EDGE_CURVE('',#2264,#2262,#1401,.T.);
#2729=EDGE_CURVE('',#2263,#2264,#1402,.T.);
#2730=EDGE_CURVE('',#2263,#2255,#1403,.T.);
#2731=EDGE_CURVE('',#2257,#2264,#1404,.T.);
#3505=ORIENTED_EDGE('',*,*,#2708,.T.);
#3506=ORIENTED_EDGE('',*,*,#2709,.F.);
#3507=ORIENTED_EDGE('',*,*,#2708,.F.);
#3508=ORIENTED_EDGE('',*,*,#2710,.T.);
#3509=ORIENTED_EDGE('',*,*,#2711,.T.);
#3510=ORIENTED_EDGE('',*,*,#2710,.F.);
#3511=ORIENTED_EDGE('',*,*,#2711,.F.);
#3512=ORIENTED_EDGE('',*,*,#2712,.F.);
#3513=ORIENTED_EDGE('',*,*,#2713,.T.);
#3514=ORIENTED_EDGE('',*,*,#2709,.T.);
#3515=ORIENTED_EDGE('',*,*,#2713,.F.);
#3516=ORIENTED_EDGE('',*,*,#2712,.T.);
#3517=ORIENTED_EDGE('',*,*,#2714,.F.);
#3518=ORIENTED_EDGE('',*,*,#2715,.T.);
#3519=ORIENTED_EDGE('',*,*,#2716,.T.);
#3520=ORIENTED_EDGE('',*,*,#2715,.F.);
#3521=ORIENTED_EDGE('',*,*,#2714,.T.);
#3522=ORIENTED_EDGE('',*,*,#2716,.F.);
#3523=ORIENTED_EDGE('',*,*,#2717,.F.);
#3524=ORIENTED_EDGE('',*,*,#2718,.T.);
#3525=ORIENTED_EDGE('',*,*,#2719,.F.);
#3526=ORIENTED_EDGE('',*,*,#2720,.F.);
#3527=ORIENTED_EDGE('',*,*,#2721,.F.);
#3528=ORIENTED_EDGE('',*,*,#2720,.T.);
#3529=ORIENTED_EDGE('',*,*,#2722,.F.);
#3530=ORIENTED_EDGE('',*,*,#2723,.F.);
#3531=ORIENTED_EDGE('',*,*,#2724,.F.);
#3532=ORIENTED_EDGE('',*,*,#2723,.T.);
#3533=ORIENTED_EDGE('',*,*,#2725,.F.);
#3534=ORIENTED_EDGE('',*,*,#2726,.F.);
#3535=ORIENTED_EDGE('',*,*,#2727,.F.);
#3536=ORIENTED_EDGE('',*,*,#2726,.T.);
#3537=ORIENTED_EDGE('',*,*,#2728,.F.);
#3538=ORIENTED_EDGE('',*,*,#2729,.F.);
#3539=ORIENTED_EDGE('',*,*,#2730,.F.);
#3540=ORIENTED_EDGE('',*,*,#2729,.T.);
#3541=ORIENTED_EDGE('',*,*,#2731,.F.);
#3542=ORIENTED_EDGE('',*,*,#2718,.F.);
#3543=ORIENTED_EDGE('',*,*,#2731,.T.);
#3544=ORIENTED_EDGE('',*,*,#2728,.T.);
#3545=ORIENTED_EDGE('',*,*,#2725,.T.);
#3546=ORIENTED_EDGE('',*,*,#2722,.T.);
#3547=ORIENTED_EDGE('',*,*,#2719,.T.);
#3548=ORIENTED_EDGE('',*,*,#2730,.T.);
#3549=ORIENTED_EDGE('',*,*,#2717,.T.);
#3550=ORIENTED_EDGE('',*,*,#2721,.T.);
#3551=ORIENTED_EDGE('',*,*,#2724,.T.);
#3552=ORIENTED_EDGE('',*,*,#2727,.T.);
#4341=CYLINDRICAL_SURFACE('',#5148,2.);
#4342=CYLINDRICAL_SURFACE('',#5151,0.685);
#4343=CYLINDRICAL_SURFACE('',#5154,1.9);
#4492=ADVANCED_FACE('',(#657,#345),#455,.T.);
#4493=ADVANCED_FACE('',(#658),#4341,.T.);
#4494=ADVANCED_FACE('',(#659),#456,.F.);
#4495=ADVANCED_FACE('',(#660),#4342,.T.);
#4496=ADVANCED_FACE('',(#661),#457,.T.);
#4497=ADVANCED_FACE('',(#662),#4343,.T.);
#4498=ADVANCED_FACE('',(#663),#458,.T.);
#4499=ADVANCED_FACE('',(#664),#459,.F.);
#4500=ADVANCED_FACE('',(#665),#460,.T.);
#4501=ADVANCED_FACE('',(#666),#461,.T.);
#4502=ADVANCED_FACE('',(#667),#462,.T.);
#4503=ADVANCED_FACE('',(#668),#463,.T.);
#4504=ADVANCED_FACE('',(#669),#464,.T.);
#4505=ADVANCED_FACE('',(#670),#465,.T.);
#4506=ADVANCED_FACE('',(#671),#466,.F.);
#4692=CLOSED_SHELL('',(#4492,#4493,#4494,#4495,#4496));
#4693=CLOSED_SHELL('',(#4497,#4498,#4499));
#4694=CLOSED_SHELL('',(#4500,#4501,#4502,#4503,#4504,#4505,#4506));
#5144=AXIS2_PLACEMENT_3D('',#8461,#5968,#5969);
#5145=AXIS2_PLACEMENT_3D('',#8462,#5970,#5971);
#5146=AXIS2_PLACEMENT_3D('',#8464,#5972,#5973);
#5147=AXIS2_PLACEMENT_3D('',#8466,#5974,#5975);
#5148=AXIS2_PLACEMENT_3D('',#8467,#5976,#5977);
#5149=AXIS2_PLACEMENT_3D('',#8470,#5979,#5980);
#5150=AXIS2_PLACEMENT_3D('',#8471,#5981,#5982);
#5151=AXIS2_PLACEMENT_3D('',#8472,#5983,#5984);
#5152=AXIS2_PLACEMENT_3D('',#8474,#5985,#5986);
#5153=AXIS2_PLACEMENT_3D('',#8476,#5988,#5989);
#5154=AXIS2_PLACEMENT_3D('',#8477,#5990,#5991);
#5155=AXIS2_PLACEMENT_3D('',#8479,#5992,#5993);
#5156=AXIS2_PLACEMENT_3D('',#8482,#5995,#5996);
#5157=AXIS2_PLACEMENT_3D('',#8483,#5997,#5998);
#5158=AXIS2_PLACEMENT_3D('',#8484,#5999,#6000);
#5159=AXIS2_PLACEMENT_3D('',#8485,#6001,#6002);
#5160=AXIS2_PLACEMENT_3D('',#8494,#6007,#6008);
#5161=AXIS2_PLACEMENT_3D('',#8500,#6012,#6013);
#5162=AXIS2_PLACEMENT_3D('',#8506,#6017,#6018);
#5163=AXIS2_PLACEMENT_3D('',#8512,#6022,#6023);
#5164=AXIS2_PLACEMENT_3D('',#8515,#6026,#6027);
#5165=AXIS2_PLACEMENT_3D('',#8516,#6028,#6029);
#5968=DIRECTION('axis',(0.,0.,1.));
#5969=DIRECTION('refdir',(1.,0.,0.));
#5970=DIRECTION('center_axis',(0.,1.,0.));
#5971=DIRECTION('ref_axis',(1.,0.,0.));
#5972=DIRECTION('center_axis',(0.,1.,0.));
#5973=DIRECTION('ref_axis',(1.,0.,0.));
#5974=DIRECTION('center_axis',(0.,1.,0.));
#5975=DIRECTION('ref_axis',(1.,0.,0.));
#5976=DIRECTION('center_axis',(0.,1.,0.));
#5977=DIRECTION('ref_axis',(1.,0.,0.));
#5978=DIRECTION('',(0.,-1.,0.));
#5979=DIRECTION('center_axis',(0.,1.,0.));
#5980=DIRECTION('ref_axis',(1.,0.,0.));
#5981=DIRECTION('center_axis',(0.,1.,0.));
#5982=DIRECTION('ref_axis',(1.,0.,0.));
#5983=DIRECTION('center_axis',(0.,1.,0.));
#5984=DIRECTION('ref_axis',(1.,0.,0.));
#5985=DIRECTION('center_axis',(0.,1.,0.));
#5986=DIRECTION('ref_axis',(1.,0.,0.));
#5987=DIRECTION('',(0.,-1.,0.));
#5988=DIRECTION('center_axis',(0.,1.,0.));
#5989=DIRECTION('ref_axis',(1.,0.,0.));
#5990=DIRECTION('center_axis',(0.,1.,0.));
#5991=DIRECTION('ref_axis',(1.,0.,0.));
#5992=DIRECTION('center_axis',(0.,1.,0.));
#5993=DIRECTION('ref_axis',(1.,0.,0.));
#5994=DIRECTION('',(0.,-1.,0.));
#5995=DIRECTION('center_axis',(0.,1.,0.));
#5996=DIRECTION('ref_axis',(1.,0.,0.));
#5997=DIRECTION('center_axis',(0.,1.,0.));
#5998=DIRECTION('ref_axis',(1.,0.,0.));
#5999=DIRECTION('center_axis',(0.,1.,0.));
#6000=DIRECTION('ref_axis',(1.,0.,0.));
#6001=DIRECTION('center_axis',(-1.,0.,0.));
#6002=DIRECTION('ref_axis',(0.,0.,1.));
#6003=DIRECTION('',(0.,0.,-1.));
#6004=DIRECTION('',(0.,1.,0.));
#6005=DIRECTION('',(0.,0.,1.));
#6006=DIRECTION('',(0.,1.,0.));
#6007=DIRECTION('center_axis',(0.,0.,-1.));
#6008=DIRECTION('ref_axis',(-1.,0.,0.));
#6009=DIRECTION('',(1.,0.,0.));
#6010=DIRECTION('',(-1.,0.,0.));
#6011=DIRECTION('',(0.,1.,0.));
#6012=DIRECTION('center_axis',(1.,0.,0.));
#6013=DIRECTION('ref_axis',(0.,0.,-1.));
#6014=DIRECTION('',(0.,0.,1.));
#6015=DIRECTION('',(0.,0.,-1.));
#6016=DIRECTION('',(0.,1.,0.));
#6017=DIRECTION('center_axis',(0.986393923832144,0.,0.164398987305357));
#6018=DIRECTION('ref_axis',(0.164398987305357,0.,-0.986393923832144));
#6019=DIRECTION('',(-0.164398987305357,0.,0.986393923832144));
#6020=DIRECTION('',(0.164398987305357,0.,-0.986393923832144));
#6021=DIRECTION('',(0.,1.,0.));
#6022=DIRECTION('center_axis',(-0.986393923832144,0.,0.164398987305357));
#6023=DIRECTION('ref_axis',(0.164398987305357,0.,0.986393923832144));
#6024=DIRECTION('',(-0.164398987305357,0.,-0.986393923832144));
#6025=DIRECTION('',(0.164398987305357,0.,0.986393923832144));
#6026=DIRECTION('center_axis',(0.,1.,0.));
#6027=DIRECTION('ref_axis',(0.,0.,1.));
#6028=DIRECTION('center_axis',(0.,1.,0.));
#6029=DIRECTION('ref_axis',(1.,0.,0.));
#8461=CARTESIAN_POINT('',(0.,0.,0.));
#8462=CARTESIAN_POINT('Origin',(0.,-5.2,2.9));
#8463=CARTESIAN_POINT('',(-2.,-5.2,2.9));
#8464=CARTESIAN_POINT('Origin',(0.,-5.2,2.9));
#8465=CARTESIAN_POINT('',(-0.685,-5.2,2.9));
#8466=CARTESIAN_POINT('Origin',(0.,-5.2,2.9));
#8467=CARTESIAN_POINT('Origin',(0.,-6.5,2.9));
#8468=CARTESIAN_POINT('',(-2.,-6.5,2.9));
#8469=CARTESIAN_POINT('',(-2.,-6.5,2.9));
#8470=CARTESIAN_POINT('Origin',(0.,-6.5,2.9));
#8471=CARTESIAN_POINT('Origin',(0.,-6.5,2.9));
#8472=CARTESIAN_POINT('Origin',(0.,-5.2,2.9));
#8473=CARTESIAN_POINT('',(-0.685,-3.6,2.9));
#8474=CARTESIAN_POINT('Origin',(0.,-3.6,2.9));
#8475=CARTESIAN_POINT('',(-0.685,-5.2,2.9));
#8476=CARTESIAN_POINT('Origin',(0.,-3.6,2.9));
#8477=CARTESIAN_POINT('Origin',(0.,-6.7,2.9));
#8478=CARTESIAN_POINT('',(-1.9,-6.5,2.9));
#8479=CARTESIAN_POINT('Origin',(0.,-6.5,2.9));
#8480=CARTESIAN_POINT('',(-1.9,-6.7,2.9));
#8481=CARTESIAN_POINT('',(-1.9,-6.7,2.9));
#8482=CARTESIAN_POINT('Origin',(0.,-6.7,2.9));
#8483=CARTESIAN_POINT('Origin',(0.,-6.5,2.9));
#8484=CARTESIAN_POINT('Origin',(0.,-6.7,2.9));
#8485=CARTESIAN_POINT('Origin',(-0.1,-6.8,1.9));
#8486=CARTESIAN_POINT('',(-0.1,-6.8,3.7));
#8487=CARTESIAN_POINT('',(-0.1,-6.8,1.9));
#8488=CARTESIAN_POINT('',(-0.1,-6.8,3.7));
#8489=CARTESIAN_POINT('',(-0.1,-6.7,3.7));
#8490=CARTESIAN_POINT('',(-0.1,-6.8,3.7));
#8491=CARTESIAN_POINT('',(-0.1,-6.7,1.9));
#8492=CARTESIAN_POINT('',(-0.1,-6.7,3.7));
#8493=CARTESIAN_POINT('',(-0.1,-6.8,1.9));
#8494=CARTESIAN_POINT('Origin',(0.1,-6.8,1.9));
#8495=CARTESIAN_POINT('',(0.1,-6.8,1.9));
#8496=CARTESIAN_POINT('',(-0.1,-6.8,1.9));
#8497=CARTESIAN_POINT('',(0.1,-6.7,1.9));
#8498=CARTESIAN_POINT('',(-0.1,-6.7,1.9));
#8499=CARTESIAN_POINT('',(0.1,-6.8,1.9));
#8500=CARTESIAN_POINT('Origin',(0.1,-6.8,3.7));
#8501=CARTESIAN_POINT('',(0.1,-6.8,3.7));
#8502=CARTESIAN_POINT('',(0.1,-6.8,1.9));
#8503=CARTESIAN_POINT('',(0.1,-6.7,3.7));
#8504=CARTESIAN_POINT('',(0.1,-6.7,1.9));
#8505=CARTESIAN_POINT('',(0.1,-6.8,3.7));
#8506=CARTESIAN_POINT('Origin',(0.,-6.8,4.3));
#8507=CARTESIAN_POINT('',(0.,-6.8,4.3));
#8508=CARTESIAN_POINT('',(0.1,-6.8,3.7));
#8509=CARTESIAN_POINT('',(0.,-6.7,4.3));
#8510=CARTESIAN_POINT('',(0.1,-6.7,3.7));
#8511=CARTESIAN_POINT('',(0.,-6.8,4.3));
#8512=CARTESIAN_POINT('Origin',(-0.1,-6.8,3.7));
#8513=CARTESIAN_POINT('',(0.,-6.8,4.3));
#8514=CARTESIAN_POINT('',(0.,-6.7,4.3));
#8515=CARTESIAN_POINT('Origin',(0.,-6.7,3.1));
#8516=CARTESIAN_POINT('Origin',(0.,-6.8,3.1));
#10221=UNCERTAINTY_MEASURE_WITH_UNIT(LENGTH_MEASURE(0.001),#10267,
'DISTANCE_ACCURACY_VALUE',
'Maximum model space distance between geometric entities at asserted c
onnectivities');
#10241=UNCERTAINTY_MEASURE_WITH_UNIT(LENGTH_MEASURE(0.001),#10267,
'DISTANCE_ACCURACY_VALUE',
'Maximum model space distance between geometric entities at asserted c
onnectivities');
#10246=(
GEOMETRIC_REPRESENTATION_CONTEXT(3)
GLOBAL_UNCERTAINTY_ASSIGNED_CONTEXT((#10221))
GLOBAL_UNIT_ASSIGNED_CONTEXT((#10267,#10269,#10270))
REPRESENTATION_CONTEXT('','3D')
);
#10266=(
GEOMETRIC_REPRESENTATION_CONTEXT(3)
GLOBAL_UNCERTAINTY_ASSIGNED_CONTEXT((#10241))
GLOBAL_UNIT_ASSIGNED_CONTEXT((#10267,#10269,#10270))
REPRESENTATION_CONTEXT('','3D')
);
#10267=(
LENGTH_UNIT()
NAMED_UNIT(*)
SI_UNIT(.CENTI.,.METRE.)
);
#10269=(
NAMED_UNIT(*)
PLANE_ANGLE_UNIT()
SI_UNIT($,.RADIAN.)
);
#10270=(
NAMED_UNIT(*)
SI_UNIT($,.STERADIAN.)
SOLID_ANGLE_UNIT()
);
#10275=SHAPE_DEFINITION_REPRESENTATION(#10299,#10358);
#10299=PRODUCT_DEFINITION_SHAPE('',$,#10383);
#10358=SHAPE_REPRESENTATION('',(#5144),#10246);
#10378=PRODUCT_DEFINITION_CONTEXT('part definition',#10452,'design');
#10383=PRODUCT_DEFINITION('Gauge dummy','Gauge dummy',#10407,
#10378);
#10407=PRODUCT_DEFINITION_FORMATION('',$,#10458);
#10452=APPLICATION_CONTEXT(
'Core Data for Automotive Mechanical Design Process');
#10453=PRODUCT_CONTEXT('part definition',#10452,'mechanical');
#10458=PRODUCT('Gauge dummy','Gauge dummy','Gauge dummy',(#10453));
#10555=COLOUR_RGB('Off White',0.89,0.88,0.83);
#10556=FILL_AREA_STYLE_COLOUR('',#10555);
#10557=FILL_AREA_STYLE('',(#10556));
#10558=SURFACE_STYLE_FILL_AREA(#10557);
#10559=SURFACE_SIDE_STYLE('',(#10558));
#10560=SURFACE_STYLE_USAGE(.BOTH.,#10559);
#10561=PRESENTATION_STYLE_ASSIGNMENT((#10560));
ENDSEC;
END-ISO-10303-21;
